ISO-10303-21;
HEADER;
/* Generated by software containing ST-Developer
 * from STEP Tools, Inc. (www.steptools.com) 
 */

FILE_DESCRIPTION(
/* description */ ('Spur gear reduction stage 2-1 on bearing plates'),
/* implementation_level */ '2;1');

FILE_NAME(
/* name */ 'Socket Set Screw - M5x8.step',
/* time_stamp */ '2026-10-28T03:22:07-07:00',
/* author */ (''),
/* organization */ (''),
/* preprocessor_version */ 'ST-DEVELOPER v20.2',
/* originating_system */ 'Autodesk Translation Framework v15.17.0.0',
/* authorisation */ '');

FILE_SCHEMA (('AUTOMOTIVE_DESIGN { 1 0 10303 214 3 1 1 }'));
ENDSEC;

DATA;
#10=MECHANICAL_DESIGN_GEOMETRIC_PRESENTATION_REPRESENTATION('',(#1004),#53909);
#856=CONICAL_SURFACE('',#12950,0.235,0.785398163397448);
#857=CONICAL_SURFACE('',#12954,0.2125,0.785398163397448);
#903=SHAPE_REPRESENTATION_RELATIONSHIP('SRR','None',#54134,#946);
#946=ADVANCED_BREP_SHAPE_REPRESENTATION('',(#1059),#53908);
#1004=STYLED_ITEM('',(#54404),#1059);
#1059=MANIFOLD_SOLID_BREP('Body1',#11331);
#1237=FACE_BOUND('',#2972,.T.);
#1494=PLANE('',#12941);
#1495=PLANE('',#12942);
#1496=PLANE('',#12943);
#1497=PLANE('',#12944);
#1498=PLANE('',#12945);
#1499=PLANE('',#12946);
#1500=PLANE('',#12947);
#1501=PLANE('',#12948);
#1502=PLANE('',#12956);
#2139=FACE_OUTER_BOUND('',#2964,.T.);
#2140=FACE_OUTER_BOUND('',#2965,.T.);
#2141=FACE_OUTER_BOUND('',#2966,.T.);
#2142=FACE_OUTER_BOUND('',#2967,.T.);
#2143=FACE_OUTER_BOUND('',#2968,.T.);
#2144=FACE_OUTER_BOUND('',#2969,.T.);
#2145=FACE_OUTER_BOUND('',#2970,.T.);
#2146=FACE_OUTER_BOUND('',#2971,.T.);
#2147=FACE_OUTER_BOUND('',#2973,.T.);
#2148=FACE_OUTER_BOUND('',#2974,.T.);
#2149=FACE_OUTER_BOUND('',#2975,.T.);
#2150=FACE_OUTER_BOUND('',#2976,.T.);
#2964=EDGE_LOOP('',(#10370,#10371,#10372,#10373));
#2965=EDGE_LOOP('',(#10374,#10375,#10376,#10377));
#2966=EDGE_LOOP('',(#10378,#10379,#10380,#10381));
#2967=EDGE_LOOP('',(#10382,#10383,#10384,#10385));
#2968=EDGE_LOOP('',(#10386,#10387,#10388,#10389));
#2969=EDGE_LOOP('',(#10390,#10391,#10392,#10393));
#2970=EDGE_LOOP('',(#10394,#10395,#10396,#10397,#10398,#10399));
#2971=EDGE_LOOP('',(#10400));
#2972=EDGE_LOOP('',(#10401,#10402,#10403,#10404,#10405,#10406));
#2973=EDGE_LOOP('',(#10407,#10408,#10409,#10410));
#2974=EDGE_LOOP('',(#10411,#10412,#10413,#10414));
#2975=EDGE_LOOP('',(#10415,#10416,#10417,#10418));
#2976=EDGE_LOOP('',(#10419));
#3597=LINE('',#53735,#4238);
#3598=LINE('',#53737,#4239);
#3599=LINE('',#53739,#4240);
#3600=LINE('',#53740,#4241);
#3601=LINE('',#53743,#4242);
#3602=LINE('',#53745,#4243);
#3603=LINE('',#53746,#4244);
#3604=LINE('',#53749,#4245);
#3605=LINE('',#53751,#4246);
#3606=LINE('',#53752,#4247);
#3607=LINE('',#53755,#4248);
#3608=LINE('',#53757,#4249);
#3609=LINE('',#53758,#4250);
#3610=LINE('',#53761,#4251);
#3611=LINE('',#53763,#4252);
#3612=LINE('',#53764,#4253);
#3613=LINE('',#53766,#4254);
#3614=LINE('',#53767,#4255);
#3615=LINE('',#53775,#4256);
#3616=LINE('',#53779,#4257);
#3617=LINE('',#53783,#4258);
#4238=VECTOR('',#15874,1.);
#4239=VECTOR('',#15875,1.);
#4240=VECTOR('',#15876,1.);
#4241=VECTOR('',#15877,1.);
#4242=VECTOR('',#15880,1.);
#4243=VECTOR('',#15881,1.);
#4244=VECTOR('',#15882,1.);
#4245=VECTOR('',#15885,1.);
#4246=VECTOR('',#15886,1.);
#4247=VECTOR('',#15887,1.);
#4248=VECTOR('',#15890,1.);
#4249=VECTOR('',#15891,1.);
#4250=VECTOR('',#15892,1.);
#4251=VECTOR('',#15895,1.);
#4252=VECTOR('',#15896,1.);
#4253=VECTOR('',#15897,1.);
#4254=VECTOR('',#15900,1.);
#4255=VECTOR('',#15901,1.);
#4256=VECTOR('',#15912,0.235);
#4257=VECTOR('',#15917,0.25);
#4258=VECTOR('',#15922,0.2125);
#4780=CIRCLE('',#12949,0.22);
#4781=CIRCLE('',#12951,0.24505);
#4782=CIRCLE('',#12953,0.24505);
#4783=CIRCLE('',#12955,0.175);
#5802=VERTEX_POINT('',#53733);
#5803=VERTEX_POINT('',#53734);
#5804=VERTEX_POINT('',#53736);
#5805=VERTEX_POINT('',#53738);
#5806=VERTEX_POINT('',#53742);
#5807=VERTEX_POINT('',#53744);
#5808=VERTEX_POINT('',#53748);
#5809=VERTEX_POINT('',#53750);
#5810=VERTEX_POINT('',#53754);
#5811=VERTEX_POINT('',#53756);
#5812=VERTEX_POINT('',#53760);
#5813=VERTEX_POINT('',#53762);
#5814=VERTEX_POINT('',#53770);
#5815=VERTEX_POINT('',#53773);
#5816=VERTEX_POINT('',#53777);
#5817=VERTEX_POINT('',#53781);
#7327=EDGE_CURVE('',#5802,#5803,#3597,.T.);
#7328=EDGE_CURVE('',#5802,#5804,#3598,.T.);
#7329=EDGE_CURVE('',#5804,#5805,#3599,.T.);
#7330=EDGE_CURVE('',#5803,#5805,#3600,.T.);
#7331=EDGE_CURVE('',#5806,#5802,#3601,.T.);
#7332=EDGE_CURVE('',#5806,#5807,#3602,.T.);
#7333=EDGE_CURVE('',#5807,#5804,#3603,.T.);
#7334=EDGE_CURVE('',#5808,#5806,#3604,.T.);
#7335=EDGE_CURVE('',#5808,#5809,#3605,.T.);
#7336=EDGE_CURVE('',#5809,#5807,#3606,.T.);
#7337=EDGE_CURVE('',#5810,#5808,#3607,.T.);
#7338=EDGE_CURVE('',#5810,#5811,#3608,.T.);
#7339=EDGE_CURVE('',#5811,#5809,#3609,.T.);
#7340=EDGE_CURVE('',#5812,#5810,#3610,.T.);
#7341=EDGE_CURVE('',#5812,#5813,#3611,.T.);
#7342=EDGE_CURVE('',#5813,#5811,#3612,.T.);
#7343=EDGE_CURVE('',#5803,#5812,#3613,.T.);
#7344=EDGE_CURVE('',#5805,#5813,#3614,.T.);
#7345=EDGE_CURVE('',#5814,#5814,#4780,.T.);
#7346=EDGE_CURVE('',#5815,#5815,#4781,.T.);
#7347=EDGE_CURVE('',#5815,#5814,#3615,.T.);
#7348=EDGE_CURVE('',#5816,#5816,#4782,.F.);
#7349=EDGE_CURVE('',#5816,#5815,#3616,.T.);
#7350=EDGE_CURVE('',#5817,#5817,#4783,.T.);
#7351=EDGE_CURVE('',#5817,#5816,#3617,.T.);
#10370=ORIENTED_EDGE('',*,*,#7327,.F.);
#10371=ORIENTED_EDGE('',*,*,#7328,.T.);
#10372=ORIENTED_EDGE('',*,*,#7329,.T.);
#10373=ORIENTED_EDGE('',*,*,#7330,.F.);
#10374=ORIENTED_EDGE('',*,*,#7331,.F.);
#10375=ORIENTED_EDGE('',*,*,#7332,.T.);
#10376=ORIENTED_EDGE('',*,*,#7333,.T.);
#10377=ORIENTED_EDGE('',*,*,#7328,.F.);
#10378=ORIENTED_EDGE('',*,*,#7334,.F.);
#10379=ORIENTED_EDGE('',*,*,#7335,.T.);
#10380=ORIENTED_EDGE('',*,*,#7336,.T.);
#10381=ORIENTED_EDGE('',*,*,#7332,.F.);
#10382=ORIENTED_EDGE('',*,*,#7337,.F.);
#10383=ORIENTED_EDGE('',*,*,#7338,.T.);
#10384=ORIENTED_EDGE('',*,*,#7339,.T.);
#10385=ORIENTED_EDGE('',*,*,#7335,.F.);
#10386=ORIENTED_EDGE('',*,*,#7340,.F.);
#10387=ORIENTED_EDGE('',*,*,#7341,.T.);
#10388=ORIENTED_EDGE('',*,*,#7342,.T.);
#10389=ORIENTED_EDGE('',*,*,#7338,.F.);
#10390=ORIENTED_EDGE('',*,*,#7343,.F.);
#10391=ORIENTED_EDGE('',*,*,#7330,.T.);
#10392=ORIENTED_EDGE('',*,*,#7344,.T.);
#10393=ORIENTED_EDGE('',*,*,#7341,.F.);
#10394=ORIENTED_EDGE('',*,*,#7344,.F.);
#10395=ORIENTED_EDGE('',*,*,#7329,.F.);
#10396=ORIENTED_EDGE('',*,*,#7333,.F.);
#10397=ORIENTED_EDGE('',*,*,#7336,.F.);
#10398=ORIENTED_EDGE('',*,*,#7339,.F.);
#10399=ORIENTED_EDGE('',*,*,#7342,.F.);
#10400=ORIENTED_EDGE('',*,*,#7345,.F.);
#10401=ORIENTED_EDGE('',*,*,#7327,.T.);
#10402=ORIENTED_EDGE('',*,*,#7343,.T.);
#10403=ORIENTED_EDGE('',*,*,#7340,.T.);
#10404=ORIENTED_EDGE('',*,*,#7337,.T.);
#10405=ORIENTED_EDGE('',*,*,#7334,.T.);
#10406=ORIENTED_EDGE('',*,*,#7331,.T.);
#10407=ORIENTED_EDGE('',*,*,#7346,.F.);
#10408=ORIENTED_EDGE('',*,*,#7347,.T.);
#10409=ORIENTED_EDGE('',*,*,#7345,.T.);
#10410=ORIENTED_EDGE('',*,*,#7347,.F.);
#10411=ORIENTED_EDGE('',*,*,#7348,.F.);
#10412=ORIENTED_EDGE('',*,*,#7349,.T.);
#10413=ORIENTED_EDGE('',*,*,#7346,.T.);
#10414=ORIENTED_EDGE('',*,*,#7349,.F.);
#10415=ORIENTED_EDGE('',*,*,#7350,.F.);
#10416=ORIENTED_EDGE('',*,*,#7351,.T.);
#10417=ORIENTED_EDGE('',*,*,#7348,.T.);
#10418=ORIENTED_EDGE('',*,*,#7351,.F.);
#10419=ORIENTED_EDGE('',*,*,#7350,.T.);
#10622=CYLINDRICAL_SURFACE('',#12952,0.24505);
#11259=ADVANCED_FACE('',(#2139),#1494,.F.);
#11260=ADVANCED_FACE('',(#2140),#1495,.F.);
#11261=ADVANCED_FACE('',(#2141),#1496,.F.);
#11262=ADVANCED_FACE('',(#2142),#1497,.F.);
#11263=ADVANCED_FACE('',(#2143),#1498,.F.);
#11264=ADVANCED_FACE('',(#2144),#1499,.F.);
#11265=ADVANCED_FACE('',(#2145),#1500,.F.);
#11266=ADVANCED_FACE('',(#2146,#1237),#1501,.T.);
#11267=ADVANCED_FACE('',(#2147),#856,.T.);
#11268=ADVANCED_FACE('',(#2148),#10622,.T.);
#11269=ADVANCED_FACE('',(#2149),#857,.T.);
#11270=ADVANCED_FACE('',(#2150),#1502,.T.);
#11331=CLOSED_SHELL('',(#11259,#11260,#11261,#11262,#11263,#11264,#11265,
#11266,#11267,#11268,#11269,#11270));
#12940=AXIS2_PLACEMENT_3D('',#53731,#15870,#15871);
#12941=AXIS2_PLACEMENT_3D('',#53732,#15872,#15873);
#12942=AXIS2_PLACEMENT_3D('',#53741,#15878,#15879);
#12943=AXIS2_PLACEMENT_3D('',#53747,#15883,#15884);
#12944=AXIS2_PLACEMENT_3D('',#53753,#15888,#15889);
#12945=AXIS2_PLACEMENT_3D('',#53759,#15893,#15894);
#12946=AXIS2_PLACEMENT_3D('',#53765,#15898,#15899);
#12947=AXIS2_PLACEMENT_3D('',#53768,#15902,#15903);
#12948=AXIS2_PLACEMENT_3D('',#53769,#15904,#15905);
#12949=AXIS2_PLACEMENT_3D('',#53771,#15906,#15907);
#12950=AXIS2_PLACEMENT_3D('',#53772,#15908,#15909);
#12951=AXIS2_PLACEMENT_3D('',#53774,#15910,#15911);
#12952=AXIS2_PLACEMENT_3D('',#53776,#15913,#15914);
#12953=AXIS2_PLACEMENT_3D('',#53778,#15915,#15916);
#12954=AXIS2_PLACEMENT_3D('',#53780,#15918,#15919);
#12955=AXIS2_PLACEMENT_3D('',#53782,#15920,#15921);
#12956=AXIS2_PLACEMENT_3D('',#53784,#15923,#15924);
#15870=DIRECTION('axis',(0.,0.,1.));
#15871=DIRECTION('refdir',(1.,0.,0.));
#15872=DIRECTION('center_axis',(0.866025403784439,0.,-0.5));
#15873=DIRECTION('ref_axis',(0.5,0.,0.866025403784439));
#15874=DIRECTION('',(0.5,0.,0.866025403784439));
#15875=DIRECTION('',(0.,-1.,0.));
#15876=DIRECTION('',(0.5,0.,0.866025403784439));
#15877=DIRECTION('',(0.,-1.,0.));
#15878=DIRECTION('center_axis',(1.92296268638356E-16,0.,-1.));
#15879=DIRECTION('ref_axis',(1.,0.,1.92296268638356E-16));
#15880=DIRECTION('',(1.,0.,1.92296268638356E-16));
#15881=DIRECTION('',(0.,-1.,0.));
#15882=DIRECTION('',(1.,0.,1.92296268638356E-16));
#15883=DIRECTION('center_axis',(-0.866025403784439,0.,-0.5));
#15884=DIRECTION('ref_axis',(0.5,0.,-0.866025403784439));
#15885=DIRECTION('',(0.5,0.,-0.866025403784439));
#15886=DIRECTION('',(0.,-1.,0.));
#15887=DIRECTION('',(0.5,0.,-0.866025403784438));
#15888=DIRECTION('center_axis',(-0.866025403784439,0.,0.5));
#15889=DIRECTION('ref_axis',(-0.5,0.,-0.866025403784439));
#15890=DIRECTION('',(-0.5,0.,-0.866025403784439));
#15891=DIRECTION('',(0.,-1.,0.));
#15892=DIRECTION('',(-0.5,0.,-0.866025403784439));
#15893=DIRECTION('center_axis',(-1.92296268638356E-16,0.,1.));
#15894=DIRECTION('ref_axis',(-1.,0.,-1.92296268638356E-16));
#15895=DIRECTION('',(-1.,0.,-1.92296268638356E-16));
#15896=DIRECTION('',(0.,-1.,0.));
#15897=DIRECTION('',(-1.,0.,-1.92296268638356E-16));
#15898=DIRECTION('center_axis',(0.866025403784439,0.,0.5));
#15899=DIRECTION('ref_axis',(-0.5,0.,0.866025403784439));
#15900=DIRECTION('',(-0.5,0.,0.866025403784439));
#15901=DIRECTION('',(-0.5,0.,0.866025403784439));
#15902=DIRECTION('center_axis',(0.,-1.,0.));
#15903=DIRECTION('ref_axis',(0.,0.,-1.));
#15904=DIRECTION('center_axis',(0.,1.,0.));
#15905=DIRECTION('ref_axis',(0.,0.,1.));
#15906=DIRECTION('center_axis',(0.,-1.,0.));
#15907=DIRECTION('ref_axis',(1.,0.,0.));
#15908=DIRECTION('center_axis',(0.,-1.,0.));
#15909=DIRECTION('ref_axis',(1.,0.,0.));
#15910=DIRECTION('center_axis',(0.,-1.,0.));
#15911=DIRECTION('ref_axis',(1.,0.,0.));
#15912=DIRECTION('',(0.707106781186547,0.707106781186548,8.65956056235493E-17));
#15913=DIRECTION('center_axis',(0.,-1.,0.));
#15914=DIRECTION('ref_axis',(1.,0.,0.));
#15915=DIRECTION('center_axis',(0.,1.,0.));
#15916=DIRECTION('ref_axis',(1.,0.,0.));
#15917=DIRECTION('',(0.,1.,0.));
#15918=DIRECTION('center_axis',(0.,1.,0.));
#15919=DIRECTION('ref_axis',(1.,0.,0.));
#15920=DIRECTION('center_axis',(0.,-1.,0.));
#15921=DIRECTION('ref_axis',(1.,0.,0.));
#15922=DIRECTION('',(-0.707106781186547,0.707106781186548,-8.65956056235493E-17));
#15923=DIRECTION('center_axis',(0.,-1.,0.));
#15924=DIRECTION('ref_axis',(0.,0.,-1.));
#53731=CARTESIAN_POINT('',(0.,0.,0.));
#53732=CARTESIAN_POINT('Origin',(0.0721687836487032,0.,-0.125));
#53733=CARTESIAN_POINT('',(0.0721687836487032,0.,-0.125));
#53734=CARTESIAN_POINT('',(0.144337567297406,0.,0.));
#53735=CARTESIAN_POINT('',(0.117710979560879,0.,-0.0461186027918559));
#53736=CARTESIAN_POINT('',(0.0721687836487032,-0.25,-0.125));
#53737=CARTESIAN_POINT('',(0.0721687836487032,0.,-0.125));
#53738=CARTESIAN_POINT('',(0.144337567297406,-0.25,0.));
#53739=CARTESIAN_POINT('',(0.144337567297406,-0.25,0.));
#53740=CARTESIAN_POINT('',(0.144337567297406,0.,0.));
#53741=CARTESIAN_POINT('Origin',(-0.0721687836487032,0.,-0.125));
#53742=CARTESIAN_POINT('',(-0.0721687836487032,0.,-0.125));
#53743=CARTESIAN_POINT('',(0.0739156081756484,0.,-0.125));
#53744=CARTESIAN_POINT('',(-0.0721687836487032,-0.25,-0.125));
#53745=CARTESIAN_POINT('',(-0.0721687836487032,0.,-0.125));
#53746=CARTESIAN_POINT('',(0.0721687836487032,-0.25,-0.125));
#53747=CARTESIAN_POINT('Origin',(-0.144337567297406,0.,-4.16333634234434E-17));
#53748=CARTESIAN_POINT('',(-0.144337567297406,0.,-1.76762539787485E-17));
#53749=CARTESIAN_POINT('',(-0.0987953713852306,0.,-0.0788813972081442));
#53750=CARTESIAN_POINT('',(-0.144337567297406,-0.25,-2.77555756156289E-17));
#53751=CARTESIAN_POINT('',(-0.144337567297406,0.,-1.76762539787485E-17));
#53752=CARTESIAN_POINT('',(-0.0721687836487032,-0.25,-0.125));
#53753=CARTESIAN_POINT('Origin',(-0.0721687836487033,0.,0.125));
#53754=CARTESIAN_POINT('',(-0.0721687836487033,0.,0.125));
#53755=CARTESIAN_POINT('',(-0.0627109795608791,0.,0.141381397208144));
#53756=CARTESIAN_POINT('',(-0.0721687836487033,-0.25,0.125));
#53757=CARTESIAN_POINT('',(-0.0721687836487033,0.,0.125));
#53758=CARTESIAN_POINT('',(-0.144337567297406,-0.25,-1.76762539787485E-17));
#53759=CARTESIAN_POINT('Origin',(0.0721687836487032,0.,0.125));
#53760=CARTESIAN_POINT('',(0.0721687836487032,0.,0.125));
#53761=CARTESIAN_POINT('',(0.146084391824352,0.,0.125));
#53762=CARTESIAN_POINT('',(0.0721687836487032,-0.25,0.125));
#53763=CARTESIAN_POINT('',(0.0721687836487032,0.,0.125));
#53764=CARTESIAN_POINT('',(-0.0721687836487033,-0.25,0.125));
#53765=CARTESIAN_POINT('Origin',(0.144337567297406,0.,0.));
#53766=CARTESIAN_POINT('',(0.153795371385231,0.,-0.0163813972081441));
#53767=CARTESIAN_POINT('',(0.0721687836487032,-0.25,0.125));
#53768=CARTESIAN_POINT('Origin',(0.,-0.25,0.));
#53769=CARTESIAN_POINT('Origin',(0.22,0.,0.));
#53770=CARTESIAN_POINT('',(-0.22,-8.67361737988404E-18,-2.69422295812418E-17));
#53771=CARTESIAN_POINT('Origin',(0.,0.,0.));
#53772=CARTESIAN_POINT('Origin',(0.,-0.015,0.));
#53773=CARTESIAN_POINT('',(-0.24505,-0.02505,-3.00099698131059E-17));
#53774=CARTESIAN_POINT('Origin',(0.,-0.02505,0.));
#53775=CARTESIAN_POINT('',(-0.235,-0.015,-2.87791997799628E-17));
#53776=CARTESIAN_POINT('Origin',(0.,-0.3775,0.));
#53777=CARTESIAN_POINT('',(-0.24505,-0.72995,3.00099698131059E-17));
#53778=CARTESIAN_POINT('Origin',(0.,-0.72995,0.));
#53779=CARTESIAN_POINT('',(-0.24505,-0.3775,-3.00099698131059E-17));
#53780=CARTESIAN_POINT('Origin',(0.,-0.7625,0.));
#53781=CARTESIAN_POINT('',(-0.175,-0.8,-2.14313189850787E-17));
#53782=CARTESIAN_POINT('Origin',(0.,-0.8,0.));
#53783=CARTESIAN_POINT('',(-0.2125,-0.7625,-2.60237444818813E-17));
#53784=CARTESIAN_POINT('Origin',(0.,-0.8,0.));
#53858=UNCERTAINTY_MEASURE_WITH_UNIT(LENGTH_MEASURE(0.001),#53910,
'DISTANCE_ACCURACY_VALUE',
'Maximum model space distance between geometric entities at asserted c
onnectivities');
#53859=UNCERTAINTY_MEASURE_WITH_UNIT(LENGTH_MEASURE(0.001),#53910,
'DISTANCE_ACCURACY_VALUE',
'Maximum model space distance between geometric entities at asserted c
onnectivities');
#53908=(
GEOMETRIC_REPRESENTATION_CONTEXT(3)
GLOBAL_UNCERTAINTY_ASSIGNED_CONTEXT((#53858))
GLOBAL_UNIT_ASSIGNED_CONTEXT((#53910,#53912,#53913))
REPRESENTATION_CONTEXT('','3D')
);
#53909=(
GEOMETRIC_REPRESENTATION_CONTEXT(3)
GLOBAL_UNCERTAINTY_ASSIGNED_CONTEXT((#53859))
GLOBAL_UNIT_ASSIGNED_CONTEXT((#53910,#53912,#53913))
REPRESENTATION_CONTEXT('','3D')
);
#53910=(
LENGTH_UNIT()
NAMED_UNIT(*)
SI_UNIT(.CENTI.,.METRE.)
);
#53912=(
NAMED_UNIT(*)
PLANE_ANGLE_UNIT()
SI_UNIT($,.RADIAN.)
);
#53913=(
NAMED_UNIT(*)
SI_UNIT($,.STERADIAN.)
SOLID_ANGLE_UNIT()
);
#53962=SHAPE_DEFINITION_REPRESENTATION(#54060,#54134);
#54060=PRODUCT_DEFINITION_SHAPE('',$,#54184);
#54134=SHAPE_REPRESENTATION('',(#12940),#53908);
#54135=PRODUCT_DEFINITION_CONTEXT('part definition',#54284,'design');
#54184=PRODUCT_DEFINITION('Socket Set Screw - M5x8',
'Socket Set Screw - M5x8',#54233,#54135);
#54233=PRODUCT_DEFINITION_FORMATION('',$,#54334);
#54284=APPLICATION_CONTEXT(
'Core Data for Automotive Mechanical Design Process');
#54285=PRODUCT_CONTEXT('part definition',#54284,'mechanical');
#54334=PRODUCT('Socket Set Screw - M5x8','Socket Set Screw - M5x8',
'Socket Set Screw - M5x8',(#54285));
#54398=COLOUR_RGB('Black',0.12,0.14,0.17);
#54399=FILL_AREA_STYLE_COLOUR('',#54398);
#54400=FILL_AREA_STYLE('',(#54399));
#54401=SURFACE_STYLE_FILL_AREA(#54400);
#54402=SURFACE_SIDE_STYLE('',(#54401));
#54403=SURFACE_STYLE_USAGE(.BOTH.,#54402);
#54404=PRESENTATION_STYLE_ASSIGNMENT((#54403));
ENDSEC;
END-ISO-10303-21;
